ISO-10303-21;
HEADER;
FILE_DESCRIPTION (('STEP AP214'),
    '1' );
FILE_NAME ('socket head cap screw_iso_ISO 4762 M6 x 60 - 24N.step',
    '2026-09-21T15:58:29',
    ( '' ),
    ( '' ),
    'SwSTEP 2.0',
    'SolidWorks 2026',
    '' );
FILE_SCHEMA (( 'AUTOMOTIVE_DESIGN' ));
ENDSEC;

DATA;
#120=ORIENTED_EDGE ( 'NONE', *, *, #22119, .T. ) ;
#173=FILL_AREA_STYLE_COLOUR ( '', #11405 ) ;
#265=VECTOR ( 'NONE', #23619, 1000.000000000000000 ) ;
#316=APPLICATION_CONTEXT ( 'automotive_design' ) ;
#368=DIRECTION ( 'NONE',  ( 0.000000000000000000, 0.000000000000000000, 1.000000000000000000 ) ) ;
#392=CARTESIAN_POINT ( 'NONE',  ( 3.000000000000000000, 1.467624384280029615, 2.541999999999997151 ) ) ;
#502=DIRECTION ( 'NONE',  ( 0.000000000000000000, 0.000000000000000000, 1.000000000000000000 ) ) ;
#595=EDGE_CURVE ( 'NONE', #13005, #8407, #4838, .T. ) ;
#608=CARTESIAN_POINT ( 'NONE',  ( 3.000000000000000000, 0.000000000000000000, 2.541999999999999815 ) ) ;
#617=FACE_OUTER_BOUND ( 'NONE', #10249, .T. ) ;
#661=ORIENTED_EDGE ( 'NONE', *, *, #1413, .T. ) ;
#689=DIRECTION ( 'NONE',  ( -0.000000000000000000, 1.625241993126352989E-15, 1.000000000000000000 ) ) ;
#789=ORIENTED_EDGE ( 'NONE', *, *, #19478, .T. ) ;
#811=ORIENTED_EDGE ( 'NONE', *, *, #30891, .F. ) ;
#890=CARTESIAN_POINT ( 'NONE',  ( 3.000000000000000000, 2.935248768560057453, -3.903127820947815962E-15 ) ) ;
#920=CARTESIAN_POINT ( 'NONE',  ( 65.44550000000002399, 0.000000000000000000, 0.000000000000000000 ) ) ;
#979=FACE_OUTER_BOUND ( 'NONE', #1371, .T. ) ;
#1035=ORIENTED_EDGE ( 'NONE', *, *, #24175, .F. ) ;
#1052=CARTESIAN_POINT ( 'NONE',  ( 66.00000000000000000, 0.000000000000000000, 0.000000000000000000 ) ) ;
#1119=LINE ( 'NONE', #4305, #27581 ) ;
#1163=EDGE_LOOP ( 'NONE', ( #23509, #19777, #32309, #19486, #17635 ) ) ;
#1172=DIRECTION ( 'NONE',  ( 0.000000000000000000, 0.000000000000000000, -1.000000000000000000 ) ) ;
#1229=ORIENTED_EDGE ( 'NONE', *, *, #4111, .F. ) ;
#1318=UNCERTAINTY_MEASURE_WITH_UNIT (LENGTH_MEASURE( 1.000000000000000082E-05 ), #23595, 'distance_accuracy_value', 'NONE');
#1371=EDGE_LOOP ( 'NONE', ( #18126, #16442, #17587, #13499, #32265 ) ) ;
#1390=ORIENTED_EDGE ( 'NONE', *, *, #19478, .F. ) ;
#1413=EDGE_CURVE ( 'NONE', #34844, #26265, #35516, .T. ) ;
#1424=TOROIDAL_SURFACE ( 'NONE', #7427, 4.700000000000000178, 0.2999999999999999889 ) ;
#1468=ORIENTED_EDGE ( 'NONE', *, *, #30969, .F. ) ;
#1505=PLANE ( 'NONE',  #24805 ) ;
#1512=VERTEX_POINT ( 'NONE', #25037 ) ;
#1521=CARTESIAN_POINT ( 'NONE',  ( 0.3000000000000016542, 0.000000000000000000, 4.700000000000000178 ) ) ;
#1777=FACE_OUTER_BOUND ( 'NONE', #33774, .T. ) ;
#1783=ORIENTED_EDGE ( 'NONE', *, *, #10181, .F. ) ;
#1793=ORIENTED_EDGE ( 'NONE', *, *, #33669, .T. ) ;
#1810=EDGE_CURVE ( 'NONE', #21528, #18894, #15223, .T. ) ;
#1870=DIRECTION ( 'NONE',  ( -0.5000000000000051070, 1.060575238724903217E-16, -0.8660254037844355990 ) ) ;
#1901=CARTESIAN_POINT ( 'NONE',  ( 0.3000000000000016542, 0.000000000000000000, 5.000000000000000000 ) ) ;
#1904=CARTESIAN_POINT ( 'NONE',  ( -31.74999999999995737, 3.673940397442060854E-16, -3.000000000000000888 ) ) ;
#1929=ADVANCED_FACE ( 'NONE', ( #19138 ), #14221, .T. ) ;
#2011=CARTESIAN_POINT ( 'NONE',  ( 3.000000000000000000, -1.467624384280027172, 2.542000000000001592 ) ) ;
#2121=CARTESIAN_POINT ( 'NONE',  ( 6.249999999999998224, 0.000000000000000000, 0.000000000000000000 ) ) ;
#2143=DIRECTION ( 'NONE',  ( -1.000000000000000000, -0.000000000000000000, -0.000000000000000000 ) ) ;
#2166=CARTESIAN_POINT ( 'NONE',  ( 66.00000000000000000, 0.000000000000000000, 2.445500000000000007 ) ) ;
#2185=CIRCLE ( 'NONE', #27310, 5.000000000000000000 ) ;
#2194=VECTOR ( 'NONE', #12838, 1000.000000000000000 ) ;
#2243=TOROIDAL_SURFACE ( 'NONE', #11230, 4.700000000000000178, 0.2999999999999999889 ) ;
#2251=( GEOMETRIC_REPRESENTATION_CONTEXT ( 3 ) GLOBAL_UNCERTAINTY_ASSIGNED_CONTEXT ( ( #7697 ) ) GLOBAL_UNIT_ASSIGNED_CONTEXT ( ( #35038, #9343, #35432 ) ) REPRESENTATION_CONTEXT ( 'NONE', 'WORKASPACE' ) );
#2286=DIRECTION ( 'NONE',  ( -1.000000000000000000, -0.000000000000000000, -0.000000000000000000 ) ) ;
#2299=VECTOR ( 'NONE', #14443, 1000.000000000000114 ) ;
#2334=CIRCLE ( 'NONE', #16098, 0.2500000000000002220 ) ;
#2429=LINE ( 'NONE', #34119, #26633 ) ;
#2591=CARTESIAN_POINT ( 'NONE',  ( 3.000000000000000000, 1.467624384280024730, -2.542000000000001592 ) ) ;
#2642=FACE_OUTER_BOUND ( 'NONE', #15803, .T. ) ;
#2716=CARTESIAN_POINT ( 'NONE',  ( 3.000000000000000000, 2.935248768560057453, -3.903127820947815962E-15 ) ) ;
#2793=LINE ( 'NONE', #11223, #30457 ) ;
#2917=FACE_OUTER_BOUND ( 'NONE', #31080, .T. ) ;
#3053=CARTESIAN_POINT ( 'NONE',  ( 0.000000000000000000, 5.939536975864662969E-16, -4.700000000000000178 ) ) ;
#3142=ORIENTED_EDGE ( 'NONE', *, *, #32210, .T. ) ;
#3165=AXIS2_PLACEMENT_3D ( 'NONE', #19480, #16307, #19308 ) ;
#3188=EDGE_CURVE ( 'NONE', #20479, #16067, #10987, .T. ) ;
#3190=DIRECTION ( 'NONE',  ( -1.000000000000000000, -0.000000000000000000, -0.000000000000000000 ) ) ;
#3246=ORIENTED_EDGE ( 'NONE', *, *, #15145, .F. ) ;
#3258=DIRECTION ( 'NONE',  ( 0.000000000000000000, 0.000000000000000000, 1.000000000000000000 ) ) ;
#3353=PRESENTATION_STYLE_ASSIGNMENT (( #26590 ) ) ;
#3355=FACE_OUTER_BOUND ( 'NONE', #13531, .T. ) ;
#3358=DIRECTION ( 'NONE',  ( -0.7071067811865382469, 8.659560562355048722E-17, -0.7071067811865568986 ) ) ;
#3389=DIRECTION ( 'NONE',  ( 1.000000000000000000, 0.000000000000000000, 0.000000000000000000 ) ) ;
#3486=ADVANCED_FACE ( 'NONE', ( #24019 ), #35464, .T. ) ;
#3563=AXIS2_PLACEMENT_3D ( 'NONE', #1052, #17740, #502 ) ;
#3604=CIRCLE ( 'NONE', #17976, 2.541999999999999815 ) ;
#3703=DIRECTION ( 'NONE',  ( 0.000000000000000000, -1.000000000000000000, 1.034244904716769672E-15 ) ) ;
#3792=CARTESIAN_POINT ( 'NONE',  ( 0.000000000000000000, -1.467624384280027172, 2.542000000000001592 ) ) ;
#3874=LINE ( 'NONE', #29386, #27318 ) ;
#3987=AXIS2_PLACEMENT_3D ( 'NONE', #4916, #2286, #8290 ) ;
#4071=CARTESIAN_POINT ( 'NONE',  ( 3.000000000000000000, 1.467624384280029615, 2.541999999999997151 ) ) ;
#4111=EDGE_CURVE ( 'NONE', #18894, #22877, #24669, .T. ) ;
#4115=ORIENTED_EDGE ( 'NONE', *, *, #24219, .F. ) ;
#4142=CARTESIAN_POINT ( 'NONE',  ( 3.000000000000000000, 2.935248768560057453, -3.903127820947815962E-15 ) ) ;
#4146=CARTESIAN_POINT ( 'NONE',  ( 3.000000000000000000, -1.467624384280027172, 2.542000000000001592 ) ) ;
#4181=CARTESIAN_POINT ( 'NONE',  ( 3.000000000000000000, 1.467624384280024730, -2.542000000000001592 ) ) ;
#4188=ORIENTED_EDGE ( 'NONE', *, *, #23547, .F. ) ;
#4189=AXIS2_PLACEMENT_3D ( 'NONE', #36663, #20143, #23142 ) ;
#4197=ORIENTED_EDGE ( 'NONE', *, *, #30648, .T. ) ;
#4238=DIRECTION ( 'NONE',  ( -1.000000000000000000, -0.000000000000000000, -0.000000000000000000 ) ) ;
#4266=AXIS2_PLACEMENT_3D ( 'NONE', #15566, #24007, #6740 ) ;
#4277=ORIENTED_EDGE ( 'NONE', *, *, #595, .T. ) ;
#4304=AXIS2_PLACEMENT_3D ( 'NONE', #19370, #22552, #36630 ) ;
#4305=CARTESIAN_POINT ( 'NONE',  ( 0.000000000000000000, 1.467624384280024730, -2.542000000000001592 ) ) ;
#4398=DIRECTION ( 'NONE',  ( 0.000000000000000000, 0.000000000000000000, 1.000000000000000000 ) ) ;
#4400=VERTEX_POINT ( 'NONE', #18230 ) ;
#4441=ORIENTED_EDGE ( 'NONE', *, *, #21818, .T. ) ;
#4593=CARTESIAN_POINT ( 'NONE',  ( 3.000000000000000000, 4.131365146527188963E-15, 2.541999999999999371 ) ) ;
#4624=FACE_OUTER_BOUND ( 'NONE', #10553, .T. ) ;
#4635=VECTOR ( 'NONE', #19266, 1000.000000000000000 ) ;
#4636=ORIENTED_EDGE ( 'NONE', *, *, #25707, .F. ) ;
#4749=CARTESIAN_POINT ( 'NONE',  ( 3.000000000000000000, 0.000000000000000000, 0.000000000000000000 ) ) ;
#4777=DIRECTION ( 'NONE',  ( 0.000000000000000000, -0.5000000000000011102, -0.8660254037844379305 ) ) ;
#4838=LINE ( 'NONE', #25091, #4635 ) ;
#4851=ADVANCED_FACE ( 'NONE', ( #12368, #6946 ), #23837, .T. ) ;
#4912=CARTESIAN_POINT ( 'NONE',  ( 6.249999999999998224, 0.000000000000000000, 0.000000000000000000 ) ) ;
#4916=CARTESIAN_POINT ( 'NONE',  ( 66.00000000000000000, 0.000000000000000000, 0.000000000000000000 ) ) ;
#5123=AXIS2_PLACEMENT_3D ( 'NONE', #19064, #30660, #7977 ) ;
#5130=LINE ( 'NONE', #28001, #33372 ) ;
#5166=MECHANICAL_DESIGN_GEOMETRIC_PRESENTATION_REPRESENTATION('',(#27994),#35709);
#5200=ORIENTED_EDGE ( 'NONE', *, *, #23436, .F. ) ;
#5288=EDGE_LOOP ( 'NONE', ( #10397, #15064, #18152, #32149 ) ) ;
#5504=DIRECTION ( 'NONE',  ( -0.000000000000000000, 0.8660254037844391517, 0.4999999999999990563 ) ) ;
#5523=EDGE_CURVE ( 'NONE', #24614, #28759, #27440, .T. ) ;
#5554=VERTEX_POINT ( 'NONE', #7112 ) ;
#5556=FACE_OUTER_BOUND ( 'NONE', #10774, .T. ) ;
#5561=PRODUCT_DEFINITION_SHAPE ( 'NONE', 'NONE',  #10927 ) ;
#5615=AXIS2_PLACEMENT_3D ( 'NONE', #14175, #19818, #8190 ) ;
#5641=ORIENTED_EDGE ( 'NONE', *, *, #9003, .F. ) ;
#5658=FACE_OUTER_BOUND ( 'NONE', #28293, .T. ) ;
#5668=DIRECTION ( 'NONE',  ( -1.000000000000000000, -0.000000000000000000, -0.000000000000000000 ) ) ;
#5734=CIRCLE ( 'NONE', #32668, 4.700000000000000178 ) ;
#5813=AXIS2_PLACEMENT_3D ( 'NONE', #29808, #15376, #10302 ) ;
#5896=VECTOR ( 'NONE', #34331, 1000.000000000000000 ) ;
#5897=CARTESIAN_POINT ( 'NONE',  ( 3.000000000000000000, 2.935248768560057453, -3.903127820947815962E-15 ) ) ;
#5961=CARTESIAN_POINT ( 'NONE',  ( 3.000000000000000000, -1.467624384280027172, 2.542000000000001592 ) ) ;
#6013=VERTEX_POINT ( 'NONE', #21861 ) ;
#6164=LINE ( 'NONE', #8803, #20855 ) ;
#6165=ORIENTED_EDGE ( 'NONE', *, *, #19629, .F. ) ;
#6338=VECTOR ( 'NONE', #30531, 1000.000000000000114 ) ;
#6488=ORIENTED_EDGE ( 'NONE', *, *, #18601, .F. ) ;
#6510=CARTESIAN_POINT ( 'NONE',  ( 3.000000000000000000, -1.467624384280027172, 2.542000000000001592 ) ) ;
#6564=ORIENTED_EDGE ( 'NONE', *, *, #32083, .T. ) ;
#6740=DIRECTION ( 'NONE',  ( 0.000000000000000000, 0.000000000000000000, 1.000000000000000000 ) ) ;
#6859=MANIFOLD_SOLID_BREP ( 'Hex', #19594 ) ;
#6946=FACE_OUTER_BOUND ( 'NONE', #26056, .T. ) ;
#6953=AXIS2_PLACEMENT_3D ( 'NONE', #11947, #26395, #26209 ) ;
#6974=DIRECTION ( 'NONE',  ( 0.000000000000000000, 0.000000000000000000, 1.000000000000000000 ) ) ;
#6993=EDGE_CURVE ( 'NONE', #9603, #8407, #1119, .T. ) ;
#7008=ORIENTED_EDGE ( 'NONE', *, *, #19898, .T. ) ;
#7044=COLOUR_RGB ( '', 0.66274510, 0.83137255, 0.94901961) ;
#7089=VECTOR ( 'NONE', #13971, 1000.000000000000114 ) ;
#7107=PLANE ( 'NONE',  #25433 ) ;
#7112=CARTESIAN_POINT ( 'NONE',  ( 66.00000000000000000, 0.000000000000000000, 2.445500000000000007 ) ) ;
#7397=DIRECTION ( 'NONE',  ( 0.000000000000000000, 0.000000000000000000, -1.000000000000000000 ) ) ;
#7423=CARTESIAN_POINT ( 'NONE',  ( 6.249999999999998224, 3.673940397442060854E-16, -3.000000000000000888 ) ) ;
#7427=AXIS2_PLACEMENT_3D ( 'NONE', #12028, #23665, #6974 ) ;
#7450=AXIS2_PLACEMENT_3D ( 'NONE', #34165, #3190, #368 ) ;
#7510=DIRECTION ( 'NONE',  ( 0.000000000000000000, 0.000000000000000000, -1.000000000000000000 ) ) ;
#7539=EDGE_CURVE ( 'NONE', #25339, #33109, #8371, .T. ) ;
#7620=DIRECTION ( 'NONE',  ( 0.000000000000000000, 1.000000000000000000, -1.224646799147353207E-16 ) ) ;
#7653=LINE ( 'NONE', #16103, #21931 ) ;
#7661=CARTESIAN_POINT ( 'NONE',  ( 3.000000000000000000, 2.935248768560057453, -3.903127820947815962E-15 ) ) ;
#7688=CARTESIAN_POINT ( 'NONE',  ( 3.000000000000000000, -2.201436576420042979, 1.271000000000003682 ) ) ;
#7697=UNCERTAINTY_MEASURE_WITH_UNIT (LENGTH_MEASURE( 1.000000000000000082E-05 ), #35038, 'distance_accuracy_value', 'NONE');
#7704=DIRECTION ( 'NONE',  ( -1.000000000000000000, -0.000000000000000000, -0.000000000000000000 ) ) ;
#7781=DIRECTION ( 'NONE',  ( 1.000000000000000000, 0.000000000000000000, 0.000000000000000000 ) ) ;
#7793=ORIENTED_EDGE ( 'NONE', *, *, #32083, .F. ) ;
#7819=AXIS2_PLACEMENT_3D ( 'NONE', #16068, #7620, #36118 ) ;
#7904=ORIENTED_EDGE ( 'NONE', *, *, #21702, .F. ) ;
#7977=DIRECTION ( 'NONE',  ( 0.000000000000000000, 0.000000000000000000, -1.000000000000000000 ) ) ;
#8003=ORIENTED_EDGE ( 'NONE', *, *, #11581, .F. ) ;
#8060=ORIENTED_EDGE ( 'NONE', *, *, #25601, .T. ) ;
#8066=ADVANCED_FACE ( 'NONE', ( #21968 ), #36579, .F. ) ;
#8070=DIRECTION ( 'NONE',  ( -1.000000000000000000, -0.000000000000000000, -0.000000000000000000 ) ) ;
#8167=DIRECTION ( 'NONE',  ( 0.000000000000000000, -0.5000000000000013323, -0.8660254037844379305 ) ) ;
#8190=DIRECTION ( 'NONE',  ( 0.000000000000000000, 0.000000000000000000, 1.000000000000000000 ) ) ;
#8235=CIRCLE ( 'NONE', #29175, 2.541999999999999815 ) ;
#8290=DIRECTION ( 'NONE',  ( 0.000000000000000000, 0.000000000000000000, 1.000000000000000000 ) ) ;
#8344=ADVANCED_FACE ( 'NONE', ( #12351 ), #32428, .T. ) ;
#8371=CIRCLE ( 'NONE', #13149, 2.541999999999999815 ) ;
#8407=VERTEX_POINT ( 'NONE', #36176 ) ;
#8429=DIRECTION ( 'NONE',  ( -1.000000000000000000, -0.000000000000000000, -0.000000000000000000 ) ) ;
#8433=VERTEX_POINT ( 'NONE', #19670 ) ;
#8499=DIRECTION ( 'NONE',  ( 0.000000000000000000, -0.4999999999999990563, 0.8660254037844391517 ) ) ;
#8580=CARTESIAN_POINT ( 'NONE',  ( 0.000000000000000000, 0.000000000000000000, 4.700000000000000178 ) ) ;
#8769=CIRCLE ( 'NONE', #30313, 3.000000000000000444 ) ;
#8803=CARTESIAN_POINT ( 'NONE',  ( 66.00000000000000000, 2.994873747314852478E-16, -2.445500000000000007 ) ) ;
#8896=CARTESIAN_POINT ( 'NONE',  ( 0.000000000000000000, 0.000000000000000000, 0.000000000000000000 ) ) ;
#8950=FACE_OUTER_BOUND ( 'NONE', #29666, .T. ) ;
#8994=ORIENTED_EDGE ( 'NONE', *, *, #15925, .T. ) ;
#9003=EDGE_CURVE ( 'NONE', #22352, #34844, #7653, .T. ) ;
#9036=CARTESIAN_POINT ( 'NONE',  ( 5.999999999999998224, 6.123233995736766282E-16, -5.000000000000000000 ) ) ;
#9083=EDGE_CURVE ( 'NONE', #21528, #16067, #21888, .T. ) ;
#9107=ADVANCED_FACE ( 'NONE', ( #18898 ), #12694, .T. ) ;
#9343=( NAMED_UNIT ( * ) PLANE_ANGLE_UNIT ( ) SI_UNIT ( $, .RADIAN. ) );
#9357=CONICAL_SURFACE ( 'NONE', #3987, 2.445500000000000007, 0.7853981633974616017 ) ;
#9481=EDGE_CURVE ( 'NONE', #4400, #5554, #36345, .T. ) ;
#9495=VECTOR ( 'NONE', #8070, 1000.000000000000000 ) ;
#9603=VERTEX_POINT ( 'NONE', #32486 ) ;
#9709=ORIENTED_EDGE ( 'NONE', *, *, #23610, .T. ) ;
#9855=VERTEX_POINT ( 'NONE', #3053 ) ;
#9928=EDGE_CURVE ( 'NONE', #22877, #12103, #20283, .T. ) ;
#9965=CARTESIAN_POINT ( 'NONE',  ( 0.3000000000000016542, 0.000000000000000000, 0.000000000000000000 ) ) ;
#10005=DIRECTION ( 'NONE',  ( 0.000000000000000000, -1.000000000000000000, 1.034244904716769672E-15 ) ) ;
#10023=CARTESIAN_POINT ( 'NONE',  ( 3.000000000000000000, 0.000000000000000000, 0.000000000000000000 ) ) ;
#10037=CARTESIAN_POINT ( 'NONE',  ( 5.999999999999998224, 0.000000000000000000, 0.000000000000000000 ) ) ;
#10104=ORIENTED_EDGE ( 'NONE', *, *, #21748, .T. ) ;
#10122=VECTOR ( 'NONE', #19232, 1000.000000000000000 ) ;
#10177=DIRECTION ( 'NONE',  ( 1.000000000000000000, 0.000000000000000000, 0.000000000000000000 ) ) ;
#10181=EDGE_CURVE ( 'NONE', #18894, #25339, #8235, .T. ) ;
#10249=EDGE_LOOP ( 'NONE', ( #17260, #29229, #31440, #1390 ) ) ;
#10296=LINE ( 'NONE', #2591, #33115 ) ;
#10302=DIRECTION ( 'NONE',  ( 0.000000000000000000, 0.000000000000000000, 1.000000000000000000 ) ) ;
#10315=ORIENTED_EDGE ( 'NONE', *, *, #24600, .T. ) ;
#10380=CARTESIAN_POINT ( 'NONE',  ( 65.44550000000002399, 0.000000000000000000, 3.000000000000000444 ) ) ;
#10397=ORIENTED_EDGE ( 'NONE', *, *, #29339, .T. ) ;
#10520=DIRECTION ( 'NONE',  ( -1.000000000000000000, -0.000000000000000000, -0.000000000000000000 ) ) ;
#10530=EDGE_LOOP ( 'NONE', ( #8994, #6488, #25480, #4115, #27817 ) ) ;
#10553=EDGE_LOOP ( 'NONE', ( #28351, #32027 ) ) ;
#10730=DIRECTION ( 'NONE',  ( -1.000000000000000000, -0.000000000000000000, -0.000000000000000000 ) ) ;
#10774=EDGE_LOOP ( 'NONE', ( #10315, #1035, #4636 ) ) ;
#10805=CARTESIAN_POINT ( 'NONE',  ( 3.000000000000000000, 0.000000000000000000, 0.000000000000000000 ) ) ;
#10824=CARTESIAN_POINT ( 'NONE',  ( 3.000000000000000000, 2.935248768560057453, -3.903127820947815962E-15 ) ) ;
#10834=ORIENTED_EDGE ( 'NONE', *, *, #24175, .T. ) ;
#10871=CARTESIAN_POINT ( 'NONE',  ( 3.000000000000000000, 1.467624384280024730, -2.542000000000001592 ) ) ;
#10878=LINE ( 'NONE', #11252, #9495 ) ;
#10895=CARTESIAN_POINT ( 'NONE',  ( 6.249999999999998224, 0.000000000000000000, 0.000000000000000000 ) ) ;
#10927=PRODUCT_DEFINITION ( 'UNKNOWN', '', #36327, #27575 ) ;
#10987=CIRCLE ( 'NONE', #31922, 2.541999999999999815 ) ;
#11163=LINE ( 'NONE', #25076, #7089 ) ;
#11165=DIRECTION ( 'NONE',  ( 1.000000000000000000, 0.000000000000000000, 0.000000000000000000 ) ) ;
#11176=DIRECTION ( 'NONE',  ( 0.000000000000000000, 0.000000000000000000, -1.000000000000000000 ) ) ;
#11223=CARTESIAN_POINT ( 'NONE',  ( 0.000000000000000000, -1.467624384280027172, 2.542000000000001592 ) ) ;
#11230=AXIS2_PLACEMENT_3D ( 'NONE', #25555, #5668, #28734 ) ;
#11249=PRODUCT ( 'socket head cap screw_iso_ISO 4762 M6 x 60 - 24N', 'socket head cap screw_iso_ISO 4762 M6 x 60 - 24N', '', ( #29372 ) ) ;
#11252=CARTESIAN_POINT ( 'NONE',  ( 3.000000000000000000, -2.935248768560059229, 3.469446951953614189E-15 ) ) ;
#11405=COLOUR_RGB ( '', 0.66274510, 0.83137255, 0.94901961) ;
#11407=EDGE_CURVE ( 'NONE', #22858, #30062, #10878, .T. ) ;
#11409=DIRECTION ( 'NONE',  ( 0.000000000000000000, -0.5000000000000011102, -0.8660254037844379305 ) ) ;
#11418=CARTESIAN_POINT ( 'NONE',  ( 3.000000000000000000, 2.935248768560057453, -3.903127820947815962E-15 ) ) ;
#11448=CARTESIAN_POINT ( 'NONE',  ( 0.000000000000000000, 2.935248768560057453, -3.903127820947815962E-15 ) ) ;
#11581=EDGE_CURVE ( 'NONE', #4400, #24614, #6164, .T. ) ;
#11596=ORIENTED_EDGE ( 'NONE', *, *, #1810, .F. ) ;
#11602=SURFACE_STYLE_USAGE ( .BOTH. , #17063 ) ;
#11676=CIRCLE ( 'NONE', #33237, 3.250000000000001332 ) ;
#11700=ORIENTED_EDGE ( 'NONE', *, *, #26945, .F. ) ;
#11935=DIRECTION ( 'NONE',  ( 0.000000000000000000, -1.000000000000000000, 1.625241993126352989E-15 ) ) ;
#11947=CARTESIAN_POINT ( 'NONE',  ( 3.000000000000000000, 0.000000000000000000, 0.000000000000000000 ) ) ;
#11981=SURFACE_STYLE_FILL_AREA ( #26247 ) ;
#12028=CARTESIAN_POINT ( 'NONE',  ( 0.3000000000000016542, 0.000000000000000000, 0.000000000000000000 ) ) ;
#12103=VERTEX_POINT ( 'NONE', #23395 ) ;
#12105=VECTOR ( 'NONE', #10520, 1000.000000000000000 ) ;
#12181=ORIENTED_EDGE ( 'NONE', *, *, #23436, .T. ) ;
#12197=ORIENTED_EDGE ( 'NONE', *, *, #25507, .T. ) ;
#12351=FACE_OUTER_BOUND ( 'NONE', #5288, .T. ) ;
#12368=FACE_BOUND ( 'NONE', #23487, .T. ) ;
#12412=CARTESIAN_POINT ( 'NONE',  ( 6.000000000000000000, 0.000000000000000000, 0.000000000000000000 ) ) ;
#12497=VERTEX_POINT ( 'NONE', #14357 ) ;
#12502=VECTOR ( 'NONE', #10005, 1000.000000000000000 ) ;
#12513=FACE_OUTER_BOUND ( 'NONE', #15944, .T. ) ;
#12529=SURFACE_STYLE_FILL_AREA ( #26786 ) ;
#12533=ORIENTED_EDGE ( 'NONE', *, *, #9083, .F. ) ;
#12694=PLANE ( 'NONE',  #27301 ) ;
#12747=FACE_OUTER_BOUND ( 'NONE', #36477, .T. ) ;
#12783=CIRCLE ( 'NONE', #7450, 4.700000000000000178 ) ;
#12838=DIRECTION ( 'NONE',  ( 0.000000000000000000, 1.000000000000000000, -1.625241993126352989E-15 ) ) ;
#12975=DIRECTION ( 'NONE',  ( -1.000000000000000000, -0.000000000000000000, -0.000000000000000000 ) ) ;
#13005=VERTEX_POINT ( 'NONE', #27866 ) ;
#13020=DIRECTION ( 'NONE',  ( 0.000000000000000000, 0.4999999999999991118, -0.8660254037844391517 ) ) ;
#13145=CARTESIAN_POINT ( 'NONE',  ( 3.000000000000000000, 2.935248768560057453, -3.903127820947815962E-15 ) ) ;
#13149=AXIS2_PLACEMENT_3D ( 'NONE', #10023, #30073, #4398 ) ;
#13378=DIRECTION ( 'NONE',  ( 0.000000000000000000, 0.000000000000000000, 1.000000000000000000 ) ) ;
#13462=APPLICATION_CONTEXT ( 'automotive_design' ) ;
#13485=VECTOR ( 'NONE', #21854, 999.9999999999998863 ) ;
#13499=ORIENTED_EDGE ( 'NONE', *, *, #36442, .F. ) ;
#13531=EDGE_LOOP ( 'NONE', ( #3246, #35756 ) ) ;
#13688=AXIS2_PLACEMENT_3D ( 'NONE', #14100, #23097, #17305 ) ;
#13769=EDGE_CURVE ( 'NONE', #25339, #22877, #20405, .T. ) ;
#13895=CYLINDRICAL_SURFACE ( 'NONE', #14766, 3.000000000000000888 ) ;
#13904=ORIENTED_EDGE ( 'NONE', *, *, #9928, .F. ) ;
#13917=ORIENTED_EDGE ( 'NONE', *, *, #25507, .F. ) ;
#13944=LINE ( 'NONE', #5897, #31509 ) ;
#13971=DIRECTION ( 'NONE',  ( 0.000000000000000000, 0.4999999999999991118, -0.8660254037844391517 ) ) ;
#14035=DIRECTION ( 'NONE',  ( 0.000000000000000000, -0.4999999999999996114, 0.8660254037844388186 ) ) ;
#14100=CARTESIAN_POINT ( 'NONE',  ( 65.44550000000002399, 0.000000000000000000, 0.000000000000000000 ) ) ;
#14158=DIRECTION ( 'NONE',  ( -1.000000000000000000, -0.000000000000000000, -0.000000000000000000 ) ) ;
#14175=CARTESIAN_POINT ( 'NONE',  ( 3.000000000000000000, 0.000000000000000000, 0.000000000000000000 ) ) ;
#14221=CYLINDRICAL_SURFACE ( 'NONE', #3165, 5.000000000000000000 ) ;
#14299=DIRECTION ( 'NONE',  ( 0.000000000000000000, -0.5000000000000013323, -0.8660254037844379305 ) ) ;
#14352=CARTESIAN_POINT ( 'NONE',  ( 0.3000000000000016542, 5.755839955992559655E-16, -4.700000000000000178 ) ) ;
#14357=CARTESIAN_POINT ( 'NONE',  ( 3.000000000000000000, -2.629050547790028157E-15, -2.541999999999999815 ) ) ;
#14443=DIRECTION ( 'NONE',  ( 0.000000000000000000, 0.4999999999999991118, -0.8660254037844391517 ) ) ;
#14505=DIRECTION ( 'NONE',  ( 0.000000000000000000, 0.000000000000000000, -1.000000000000000000 ) ) ;
#14670=ADVANCED_FACE ( 'NONE', ( #19319 ), #18761, .F. ) ;
#14753=VERTEX_POINT ( 'NONE', #10871 ) ;
#14763=FACE_OUTER_BOUND ( 'NONE', #32453, .T. ) ;
#14766=AXIS2_PLACEMENT_3D ( 'NONE', #22168, #10730, #25341 ) ;
#14793=PLANE ( 'NONE',  #33817 ) ;
#14815=DIRECTION ( 'NONE',  ( 1.000000000000000000, 0.000000000000000000, 0.000000000000000000 ) ) ;
#14866=DIRECTION ( 'NONE',  ( 0.000000000000000000, -0.4999999999999996114, 0.8660254037844388186 ) ) ;
#14988=SHAPE_REPRESENTATION_RELATIONSHIP ( 'NONE' , 'NONE' ,  #33015, #17512 ) ;
#15049=DIRECTION ( 'NONE',  ( 0.000000000000000000, -1.034244904716769672E-15, -1.000000000000000000 ) ) ;
#15064=ORIENTED_EDGE ( 'NONE', *, *, #18233, .T. ) ;
#15145=EDGE_CURVE ( 'NONE', #5554, #4400, #26314, .T. ) ;
#15174=DIRECTION ( 'NONE',  ( 0.000000000000000000, -0.5000000000000013323, -0.8660254037844379305 ) ) ;
#15223=LINE ( 'NONE', #23490, #31152 ) ;
#15304=CARTESIAN_POINT ( 'NONE',  ( 3.000000000000000000, 2.201436576420042535, 1.270999999999998353 ) ) ;
#15376=DIRECTION ( 'NONE',  ( -1.000000000000000000, -0.000000000000000000, -0.000000000000000000 ) ) ;
#15410=ORIENTED_EDGE ( 'NONE', *, *, #29339, .F. ) ;
#15419=AXIS2_PLACEMENT_3D ( 'NONE', #10037, #4238, #36283 ) ;
#15441=AXIS2_PLACEMENT_3D ( 'NONE', #4181, #15049, #18043 ) ;
#15468=ADVANCED_FACE ( 'NONE', ( #2917 ), #20341, .T. ) ;
#15566=CARTESIAN_POINT ( 'NONE',  ( -31.74999999999995737, 0.000000000000000000, 0.000000000000000000 ) ) ;
#15800=AXIS2_PLACEMENT_3D ( 'NONE', #25909, #24859, #23093 ) ;
#15803=EDGE_LOOP ( 'NONE', ( #25610, #30119, #15410, #7904 ) ) ;
#15925=EDGE_CURVE ( 'NONE', #6013, #9603, #36623, .T. ) ;
#15933=DIRECTION ( 'NONE',  ( 0.000000000000000000, -1.000000000000000000, 0.000000000000000000 ) ) ;
#15944=EDGE_LOOP ( 'NONE', ( #30308, #25258, #22638 ) ) ;
#15991=DIRECTION ( 'NONE',  ( 0.000000000000000000, 0.000000000000000000, 1.000000000000000000 ) ) ;
#15996=VECTOR ( 'NONE', #34901, 1000.000000000000000 ) ;
#16014=CIRCLE ( 'NONE', #5813, 5.000000000000000000 ) ;
#16067=VERTEX_POINT ( 'NONE', #7688 ) ;
#16068=CARTESIAN_POINT ( 'NONE',  ( 6.249999999999998224, 3.980102097228899218E-16, 3.250000000000001332 ) ) ;
#16098=AXIS2_PLACEMENT_3D ( 'NONE', #24744, #15933, #19137 ) ;
#16103=CARTESIAN_POINT ( 'NONE',  ( -31.74999999999995737, 6.123233995736766282E-16, -5.000000000000000000 ) ) ;
#16259=ORIENTED_EDGE ( 'NONE', *, *, #32824, .F. ) ;
#16307=DIRECTION ( 'NONE',  ( -1.000000000000000000, -0.000000000000000000, -0.000000000000000000 ) ) ;
#16325=DIRECTION ( 'NONE',  ( 0.000000000000000000, 0.000000000000000000, 1.000000000000000000 ) ) ;
#16366=VECTOR ( 'NONE', #14866, 1000.000000000000000 ) ;
#16442=ORIENTED_EDGE ( 'NONE', *, *, #595, .F. ) ;
#16480=AXIS2_PLACEMENT_3D ( 'NONE', #17363, #11165, #34067 ) ;
#16481=CARTESIAN_POINT ( 'NONE',  ( 3.000000000000000000, 3.113052163432572109E-16, -2.541999999999999815 ) ) ;
#16703=CARTESIAN_POINT ( 'NONE',  ( 3.000000000000000000, 0.000000000000000000, 0.000000000000000000 ) ) ;
#16753=CARTESIAN_POINT ( 'NONE',  ( 0.000000000000000000, 2.935248768560057453, -3.903127820947815962E-15 ) ) ;
#16931=DIRECTION ( 'NONE',  ( 0.000000000000000000, 0.000000000000000000, -1.000000000000000000 ) ) ;
#16950=VERTEX_POINT ( 'NONE', #8580 ) ;
#17063=SURFACE_SIDE_STYLE ('',( #11981 ) ) ;
#17168=DIRECTION ( 'NONE',  ( 0.000000000000000000, 0.000000000000000000, 1.000000000000000000 ) ) ;
#17260=ORIENTED_EDGE ( 'NONE', *, *, #21818, .F. ) ;
#17269=CARTESIAN_POINT ( 'NONE',  ( 3.000000000000000000, -2.935248768560059229, 3.469446951953614189E-15 ) ) ;
#17305=DIRECTION ( 'NONE',  ( 0.000000000000000000, 0.000000000000000000, 1.000000000000000000 ) ) ;
#17363=CARTESIAN_POINT ( 'NONE',  ( 6.249999999999998224, 0.000000000000000000, 0.000000000000000000 ) ) ;
#17512=ADVANCED_BREP_SHAPE_REPRESENTATION ( '', ( #6859, #21385 ), #2251 ) ;
#17587=ORIENTED_EDGE ( 'NONE', *, *, #24600, .F. ) ;
#17635=ORIENTED_EDGE ( 'NONE', *, *, #9928, .T. ) ;
#17727=AXIS2_PLACEMENT_3D ( 'NONE', #37050, #34411, #34240 ) ;
#17740=DIRECTION ( 'NONE',  ( -1.000000000000000000, -0.000000000000000000, -0.000000000000000000 ) ) ;
#17824=DIRECTION ( 'NONE',  ( 0.000000000000000000, 0.8660254037844380415, -0.5000000000000012212 ) ) ;
#17976=AXIS2_PLACEMENT_3D ( 'NONE', #10805, #14158, #17168 ) ;
#17998=DIRECTION ( 'NONE',  ( 0.000000000000000000, 0.000000000000000000, 1.000000000000000000 ) ) ;
#18043=DIRECTION ( 'NONE',  ( 0.000000000000000000, 1.000000000000000000, -1.034244904716769672E-15 ) ) ;
#18126=ORIENTED_EDGE ( 'NONE', *, *, #6993, .T. ) ;
#18152=ORIENTED_EDGE ( 'NONE', *, *, #26945, .T. ) ;
#18154=DIRECTION ( 'NONE',  ( 0.000000000000000000, 0.000000000000000000, -1.000000000000000000 ) ) ;
#18167=CARTESIAN_POINT ( 'NONE',  ( 3.000000000000000000, 2.935248768560057453, -3.903127820947815962E-15 ) ) ;
#18230=CARTESIAN_POINT ( 'NONE',  ( 66.00000000000000000, 3.334407072378456173E-16, -2.445500000000000007 ) ) ;
#18233=EDGE_CURVE ( 'NONE', #24614, #28371, #33029, .T. ) ;
#18268=LINE ( 'NONE', #21826, #36302 ) ;
#18272=AXIS2_PLACEMENT_3D ( 'NONE', #890, #20766, #23974 ) ;
#18327=CONICAL_SURFACE ( 'NONE', #6953, 2.541999999999999815, 1.047197551196591858 ) ;
#18554=DIRECTION ( 'NONE',  ( 0.000000000000000000, 0.8660254037844379305, -0.5000000000000014433 ) ) ;
#18601=EDGE_CURVE ( 'NONE', #14753, #9603, #10296, .T. ) ;
#18642=ORIENTED_EDGE ( 'NONE', *, *, #21702, .T. ) ;
#18686=FACE_BOUND ( 'NONE', #31863, .T. ) ;
#18710=CARTESIAN_POINT ( 'NONE',  ( 4.467624384280048488, 0.000000000000000000, 0.000000000000000000 ) ) ;
#18761=PLANE ( 'NONE',  #32952 ) ;
#18849=EDGE_LOOP ( 'NONE', ( #13917, #11700, #20238, #20891 ) ) ;
#18894=VERTEX_POINT ( 'NONE', #4593 ) ;
#18898=FACE_OUTER_BOUND ( 'NONE', #1163, .T. ) ;
#18964=ADVANCED_FACE ( 'NONE', ( #1777 ), #27635, .F. ) ;
#19036=AXIS2_PLACEMENT_3D ( 'NONE', #2121, #28186, #16931 ) ;
#19064=CARTESIAN_POINT ( 'NONE',  ( 6.000000000000000000, 5.000000000000000000, 0.000000000000000000 ) ) ;
#19084=EDGE_CURVE ( 'NONE', #8433, #25339, #28746, .T. ) ;
#19114=DIRECTION ( 'NONE',  ( 0.000000000000000000, 0.5000000000000013323, 0.8660254037844378194 ) ) ;
#19137=DIRECTION ( 'NONE',  ( 0.000000000000000000, 0.000000000000000000, -1.000000000000000000 ) ) ;
#19138=FACE_OUTER_BOUND ( 'NONE', #26749, .T. ) ;
#19157=DIRECTION ( 'NONE',  ( 1.000000000000000000, 0.000000000000000000, 0.000000000000000000 ) ) ;
#19159=VERTEX_POINT ( 'NONE', #31893 ) ;
#19191=( GEOMETRIC_REPRESENTATION_CONTEXT ( 3 ) GLOBAL_UNCERTAINTY_ASSIGNED_CONTEXT ( ( #36575 ) ) GLOBAL_UNIT_ASSIGNED_CONTEXT ( ( #26051, #31307, #31681 ) ) REPRESENTATION_CONTEXT ( 'NONE', 'WORKASPACE' ) );
#19197=ORIENTED_EDGE ( 'NONE', *, *, #25601, .F. ) ;
#19232=DIRECTION ( 'NONE',  ( 0.000000000000000000, 1.000000000000000000, -1.625241993126352989E-15 ) ) ;
#19266=DIRECTION ( 'NONE',  ( -1.000000000000000000, -0.000000000000000000, -0.000000000000000000 ) ) ;
#19273=ADVANCED_FACE ( 'NONE', ( #617 ), #1424, .T. ) ;
#19281=ADVANCED_FACE ( 'NONE', ( #32467 ), #33768, .F. ) ;
#19308=DIRECTION ( 'NONE',  ( 0.000000000000000000, 0.000000000000000000, 1.000000000000000000 ) ) ;
#19319=FACE_OUTER_BOUND ( 'NONE', #23071, .T. ) ;
#19353=ORIENTED_EDGE ( 'NONE', *, *, #10181, .T. ) ;
#19370=CARTESIAN_POINT ( 'NONE',  ( 3.000000000000000000, 0.000000000000000000, 0.000000000000000000 ) ) ;
#19399=CARTESIAN_POINT ( 'NONE',  ( 3.000000000000000000, -1.467624384280027172, 2.542000000000001592 ) ) ;
#19478=EDGE_CURVE ( 'NONE', #9855, #16950, #12783, .T. ) ;
#19480=CARTESIAN_POINT ( 'NONE',  ( -31.74999999999995737, 0.000000000000000000, 0.000000000000000000 ) ) ;
#19483=LINE ( 'NONE', #16481, #20782 ) ;
#19486=ORIENTED_EDGE ( 'NONE', *, *, #13769, .T. ) ;
#19594=CLOSED_SHELL ( 'NONE', ( #31357, #22271, #8066, #33387, #8344, #1929, #4851, #20406, #21678, #33411, #15468, #21016, #19281, #19273, #9107, #25396, #3486, #28868, #30190, #21142, #31346, #18964, #31867, #20742, #32349, #14670, #36381 ) ) ;
#19615=VECTOR ( 'NONE', #31888, 1000.000000000000114 ) ;
#19629=EDGE_CURVE ( 'NONE', #21528, #34463, #32608, .T. ) ;
#19670=CARTESIAN_POINT ( 'NONE',  ( 3.000000000000000000, 2.935248768560057453, -3.903127820947815962E-15 ) ) ;
#19777=ORIENTED_EDGE ( 'NONE', *, *, #34282, .F. ) ;
#19798=STYLED_ITEM ( 'NONE', ( #34156 ), #6859 ) ;
#19818=DIRECTION ( 'NONE',  ( -1.000000000000000000, -0.000000000000000000, -0.000000000000000000 ) ) ;
#19852=AXIS2_PLACEMENT_3D ( 'NONE', #4146, #17824, #29258 ) ;
#19866=ORIENTED_EDGE ( 'NONE', *, *, #36770, .F. ) ;
#19898=EDGE_CURVE ( 'NONE', #28759, #26995, #2429, .T. ) ;
#20022=DIRECTION ( 'NONE',  ( -1.000000000000000000, -0.000000000000000000, -0.000000000000000000 ) ) ;
#20065=DIRECTION ( 'NONE',  ( 0.000000000000000000, 0.000000000000000000, -1.000000000000000000 ) ) ;
#20143=DIRECTION ( 'NONE',  ( -1.000000000000000000, -0.000000000000000000, -0.000000000000000000 ) ) ;
#20238=ORIENTED_EDGE ( 'NONE', *, *, #30891, .T. ) ;
#20283=LINE ( 'NONE', #392, #15996 ) ;
#20308=CARTESIAN_POINT ( 'NONE',  ( 3.000000000000000000, 2.935248768560057453, -3.903127820947815962E-15 ) ) ;
#20341=CONICAL_SURFACE ( 'NONE', #4189, 2.445500000000000007, 0.7853981633974616017 ) ;
#20405=LINE ( 'NONE', #11418, #30489 ) ;
#20406=ADVANCED_FACE ( 'NONE', ( #5658 ), #22052, .T. ) ;
#20429=LINE ( 'NONE', #17269, #2299 ) ;
#20476=DIRECTION ( 'NONE',  ( 0.000000000000000000, 1.000000000000000000, -1.625241993126352989E-15 ) ) ;
#20479=VERTEX_POINT ( 'NONE', #25547 ) ;
#20615=CARTESIAN_POINT ( 'NONE',  ( 0.3000000000000016542, 6.123233995736766282E-16, -5.000000000000000000 ) ) ;
#20680=AXIS2_PLACEMENT_3D ( 'NONE', #14352, #22967, #26148 ) ;
#20742=ADVANCED_FACE ( 'NONE', ( #12747 ), #1505, .F. ) ;
#20766=DIRECTION ( 'NONE',  ( 1.000000000000000000, 0.000000000000000000, 0.000000000000000000 ) ) ;
#20781=FILL_AREA_STYLE_COLOUR ( '', #7044 ) ;
#20782=VECTOR ( 'NONE', #1870, 1000.000000000000114 ) ;
#20855=VECTOR ( 'NONE', #3358, 999.9999999999998863 ) ;
#20891=ORIENTED_EDGE ( 'NONE', *, *, #34466, .F. ) ;
#20972=AXIS2_PLACEMENT_3D ( 'NONE', #6510, #689, #11935 ) ;
#21015=DIRECTION ( 'NONE',  ( -0.000000000000000000, 0.000000000000000000, 1.000000000000000000 ) ) ;
#21016=ADVANCED_FACE ( 'NONE', ( #3355 ), #14793, .T. ) ;
#21065=ORIENTED_EDGE ( 'NONE', *, *, #18233, .F. ) ;
#21142=ADVANCED_FACE ( 'NONE', ( #35986 ), #7107, .F. ) ;
#21385=AXIS2_PLACEMENT_3D ( 'NONE', #8896, #30384, #36396 ) ;
#21409=DIRECTION ( 'NONE',  ( 1.000000000000000000, 0.000000000000000000, 0.000000000000000000 ) ) ;
#21507=ORIENTED_EDGE ( 'NONE', *, *, #1810, .T. ) ;
#21528=VERTEX_POINT ( 'NONE', #5961 ) ;
#21678=ADVANCED_FACE ( 'NONE', ( #18686, #4624 ), #35947, .T. ) ;
#21702=EDGE_CURVE ( 'NONE', #5554, #28759, #28391, .T. ) ;
#21705=DIRECTION ( 'NONE',  ( 0.000000000000000000, -0.8660254037844388186, -0.4999999999999997224 ) ) ;
#21748=EDGE_CURVE ( 'NONE', #33109, #14753, #33297, .T. ) ;
#21780=CONICAL_SURFACE ( 'NONE', #5615, 2.541999999999999815, 1.047197551196591858 ) ;
#21818=EDGE_CURVE ( 'NONE', #34844, #9855, #36864, .T. ) ;
#21826=CARTESIAN_POINT ( 'NONE',  ( 3.000000000000000000, -2.935248768560059229, 3.469446951953614189E-15 ) ) ;
#21854=DIRECTION ( 'NONE',  ( -0.7071067811865382469, 0.000000000000000000, 0.7071067811865568986 ) ) ;
#21861=CARTESIAN_POINT ( 'NONE',  ( 0.000000000000000000, 2.935248768560057453, -3.903127820947815962E-15 ) ) ;
#21888=LINE ( 'NONE', #2011, #6338 ) ;
#21931=VECTOR ( 'NONE', #35786, 1000.000000000000000 ) ;
#21941=CARTESIAN_POINT ( 'NONE',  ( 3.000000000000000000, 2.935248768560057453, -3.903127820947815962E-15 ) ) ;
#21968=FACE_OUTER_BOUND ( 'NONE', #24052, .T. ) ;
#22019=CARTESIAN_POINT ( 'NONE',  ( 3.000000000000000000, 2.935248768560057453, -3.903127820947815962E-15 ) ) ;
#22052=CYLINDRICAL_SURFACE ( 'NONE', #15800, 5.000000000000000000 ) ;
#22119=EDGE_CURVE ( 'NONE', #16067, #18894, #27634, .T. ) ;
#22131=DIRECTION ( 'NONE',  ( 0.000000000000000000, 0.000000000000000000, -1.000000000000000000 ) ) ;
#22168=CARTESIAN_POINT ( 'NONE',  ( -31.74999999999995737, 0.000000000000000000, 0.000000000000000000 ) ) ;
#22271=ADVANCED_FACE ( 'NONE', ( #28349 ), #2243, .T. ) ;
#22352=VERTEX_POINT ( 'NONE', #9036 ) ;
#22489=ORIENTED_EDGE ( 'NONE', *, *, #32824, .T. ) ;
#22521=LINE ( 'NONE', #11448, #5896 ) ;
#22552=DIRECTION ( 'NONE',  ( -1.000000000000000000, -0.000000000000000000, -0.000000000000000000 ) ) ;
#22561=PLANE ( 'NONE',  #32049 ) ;
#22638=ORIENTED_EDGE ( 'NONE', *, *, #7539, .F. ) ;
#22706=EDGE_LOOP ( 'NONE', ( #1468, #6165, #24699, #12181, #28227 ) ) ;
#22799=MECHANICAL_DESIGN_GEOMETRIC_PRESENTATION_REPRESENTATION('',(#19798),#19191);
#22858=VERTEX_POINT ( 'NONE', #35758 ) ;
#22877=VERTEX_POINT ( 'NONE', #4071 ) ;
#22967=DIRECTION ( 'NONE',  ( -0.000000000000000000, 1.000000000000000000, 1.224646799147353207E-16 ) ) ;
#22998=ORIENTED_EDGE ( 'NONE', *, *, #4111, .T. ) ;
#23045=DIRECTION ( 'NONE',  ( 1.000000000000000000, 0.000000000000000000, 0.000000000000000000 ) ) ;
#23071=EDGE_LOOP ( 'NONE', ( #10104, #24542, #19197 ) ) ;
#23077=EDGE_CURVE ( 'NONE', #30062, #8407, #11163, .T. ) ;
#23093=DIRECTION ( 'NONE',  ( 0.000000000000000000, 0.000000000000000000, 1.000000000000000000 ) ) ;
#23097=DIRECTION ( 'NONE',  ( -1.000000000000000000, -0.000000000000000000, -0.000000000000000000 ) ) ;
#23142=DIRECTION ( 'NONE',  ( 0.000000000000000000, 0.000000000000000000, 1.000000000000000000 ) ) ;
#23258=ORIENTED_EDGE ( 'NONE', *, *, #23610, .F. ) ;
#23395=CARTESIAN_POINT ( 'NONE',  ( 0.000000000000000000, 1.467624384280029615, 2.541999999999997151 ) ) ;
#23436=EDGE_CURVE ( 'NONE', #16067, #22858, #5130, .T. ) ;
#23487=EDGE_LOOP ( 'NONE', ( #4197, #19866, #25190, #26668, #36243, #25669 ) ) ;
#23490=CARTESIAN_POINT ( 'NONE',  ( 3.000000000000000000, -1.467624384280027172, 2.542000000000001592 ) ) ;
#23509=ORIENTED_EDGE ( 'NONE', *, *, #30648, .F. ) ;
#23547=EDGE_CURVE ( 'NONE', #26995, #28371, #36985, .T. ) ;
#23594=ORIENTED_EDGE ( 'NONE', *, *, #3188, .T. ) ;
#23595=( LENGTH_UNIT ( ) NAMED_UNIT ( * ) SI_UNIT ( .MILLI., .METRE. ) );
#23610=EDGE_CURVE ( 'NONE', #35409, #18894, #25761, .T. ) ;
#23619=DIRECTION ( 'NONE',  ( -1.000000000000000000, -0.000000000000000000, -0.000000000000000000 ) ) ;
#23665=DIRECTION ( 'NONE',  ( -1.000000000000000000, -0.000000000000000000, -0.000000000000000000 ) ) ;
#23670=ORIENTED_EDGE ( 'NONE', *, *, #34466, .T. ) ;
#23690=DIRECTION ( 'NONE',  ( -1.000000000000000000, -0.000000000000000000, -0.000000000000000000 ) ) ;
#23710=CIRCLE ( 'NONE', #30288, 0.2999999999999999334 ) ;
#23837=PLANE ( 'NONE',  #24330 ) ;
#23892=ORIENTED_EDGE ( 'NONE', *, *, #1413, .F. ) ;
#23903=LINE ( 'NONE', #35518, #12502 ) ;
#23974=DIRECTION ( 'NONE',  ( 0.000000000000000000, 0.000000000000000000, -1.000000000000000000 ) ) ;
#23987=SURFACE_SIDE_STYLE ('',( #12529 ) ) ;
#24007=DIRECTION ( 'NONE',  ( -1.000000000000000000, -0.000000000000000000, -0.000000000000000000 ) ) ;
#24019=FACE_OUTER_BOUND ( 'NONE', #22706, .T. ) ;
#24052=EDGE_LOOP ( 'NONE', ( #4188, #12197, #7793, #811 ) ) ;
#24148=CARTESIAN_POINT ( 'NONE',  ( 3.000000000000000000, 2.935248768560057453, -3.903127820947815962E-15 ) ) ;
#24175=EDGE_CURVE ( 'NONE', #20479, #13005, #20429, .T. ) ;
#24219=EDGE_CURVE ( 'NONE', #8433, #33109, #29597, .T. ) ;
#24330=AXIS2_PLACEMENT_3D ( 'NONE', #27180, #34899, #21015 ) ;
#24366=DIRECTION ( 'NONE',  ( 0.000000000000000000, -1.000000000000000000, 1.034244904716769672E-15 ) ) ;
#24542=ORIENTED_EDGE ( 'NONE', *, *, #36442, .T. ) ;
#24600=EDGE_CURVE ( 'NONE', #12497, #13005, #23903, .T. ) ;
#24614=VERTEX_POINT ( 'NONE', #32888 ) ;
#24669=LINE ( 'NONE', #19399, #10122 ) ;
#24699=ORIENTED_EDGE ( 'NONE', *, *, #9083, .T. ) ;
#24728=AXIS2_PLACEMENT_3D ( 'NONE', #36647, #7781, #13378 ) ;
#24744=CARTESIAN_POINT ( 'NONE',  ( 6.249999999999998224, 0.000000000000000000, -3.250000000000001332 ) ) ;
#24750=CARTESIAN_POINT ( 'NONE',  ( 6.000000000000000000, 0.000000000000000000, 0.000000000000000000 ) ) ;
#24794=AXIS2_PLACEMENT_3D ( 'NONE', #10824, #31411, #11176 ) ;
#24805=AXIS2_PLACEMENT_3D ( 'NONE', #13145, #19157, #7510 ) ;
#24859=DIRECTION ( 'NONE',  ( -1.000000000000000000, -0.000000000000000000, -0.000000000000000000 ) ) ;
#24872=CIRCLE ( 'NONE', #16480, 3.000000000000000888 ) ;
#24980=DIRECTION ( 'NONE',  ( 0.000000000000000000, 0.000000000000000000, -1.000000000000000000 ) ) ;
#25037=CARTESIAN_POINT ( 'NONE',  ( 5.999999999999999112, 3.980102097228899218E-16, 3.250000000000001332 ) ) ;
#25076=CARTESIAN_POINT ( 'NONE',  ( 0.000000000000000000, -2.935248768560059229, 3.469446951953614189E-15 ) ) ;
#25091=CARTESIAN_POINT ( 'NONE',  ( 3.000000000000000000, -1.467624384280032501, -2.541999999999998483 ) ) ;
#25182=ORIENTED_EDGE ( 'NONE', *, *, #25707, .T. ) ;
#25190=ORIENTED_EDGE ( 'NONE', *, *, #30969, .T. ) ;
#25258=ORIENTED_EDGE ( 'NONE', *, *, #24219, .T. ) ;
#25339=VERTEX_POINT ( 'NONE', #15304 ) ;
#25341=DIRECTION ( 'NONE',  ( 0.000000000000000000, 0.000000000000000000, 1.000000000000000000 ) ) ;
#25360=AXIS2_PLACEMENT_3D ( 'NONE', #22019, #33821, #7397 ) ;
#25396=ADVANCED_FACE ( 'NONE', ( #8950 ), #31797, .F. ) ;
#25433=AXIS2_PLACEMENT_3D ( 'NONE', #7661, #18554, #19114 ) ;
#25480=ORIENTED_EDGE ( 'NONE', *, *, #21748, .F. ) ;
#25507=EDGE_CURVE ( 'NONE', #26995, #1512, #29938, .T. ) ;
#25524=FACE_OUTER_BOUND ( 'NONE', #25949, .T. ) ;
#25547=CARTESIAN_POINT ( 'NONE',  ( 3.000000000000000000, -2.201436576420045643, -1.270999999999998575 ) ) ;
#25555=CARTESIAN_POINT ( 'NONE',  ( 0.3000000000000016542, 0.000000000000000000, 0.000000000000000000 ) ) ;
#25601=EDGE_CURVE ( 'NONE', #33109, #12497, #3604, .T. ) ;
#25610=ORIENTED_EDGE ( 'NONE', *, *, #15145, .T. ) ;
#25629=CIRCLE ( 'NONE', #15419, 5.000000000000000000 ) ;
#25634=FACE_OUTER_BOUND ( 'NONE', #35536, .T. ) ;
#25669=ORIENTED_EDGE ( 'NONE', *, *, #15925, .F. ) ;
#25707=EDGE_CURVE ( 'NONE', #12497, #20479, #27307, .T. ) ;
#25761=LINE ( 'NONE', #608, #19615 ) ;
#25909=CARTESIAN_POINT ( 'NONE',  ( -31.74999999999995737, 0.000000000000000000, 0.000000000000000000 ) ) ;
#25949=EDGE_LOOP ( 'NONE', ( #21065, #34527, #7008, #35795 ) ) ;
#25978=CARTESIAN_POINT ( 'NONE',  ( 0.000000000000000000, 0.000000000000000000, 0.000000000000000000 ) ) ;
#26040=CARTESIAN_POINT ( 'NONE',  ( 66.00000000000000000, 2.445500000000000007, 0.000000000000000000 ) ) ;
#26051=( LENGTH_UNIT ( ) NAMED_UNIT ( * ) SI_UNIT ( .MILLI., .METRE. ) );
#26056=EDGE_LOOP ( 'NONE', ( #29392, #789 ) ) ;
#26148=DIRECTION ( 'NONE',  ( 0.000000000000000000, -1.224646799147353207E-16, 1.000000000000000000 ) ) ;
#26209=DIRECTION ( 'NONE',  ( 0.000000000000000000, 0.000000000000000000, 1.000000000000000000 ) ) ;
#26247=FILL_AREA_STYLE ('',( #173 ) ) ;
#26258=CARTESIAN_POINT ( 'NONE',  ( 3.000000000000000000, -1.467624384280027172, 2.542000000000001592 ) ) ;
#26265=VERTEX_POINT ( 'NONE', #1901 ) ;
#26267=DIRECTION ( 'NONE',  ( 0.000000000000000000, 0.000000000000000000, -1.000000000000000000 ) ) ;
#26314=CIRCLE ( 'NONE', #3563, 2.445500000000000007 ) ;
#26395=DIRECTION ( 'NONE',  ( -1.000000000000000000, -0.000000000000000000, -0.000000000000000000 ) ) ;
#26431=DIRECTION ( 'NONE',  ( -1.000000000000000000, -0.000000000000000000, -0.000000000000000000 ) ) ;
#26590=SURFACE_STYLE_USAGE ( .BOTH. , #23987 ) ;
#26633=VECTOR ( 'NONE', #20022, 1000.000000000000000 ) ;
#26644=ORIENTED_EDGE ( 'NONE', *, *, #11407, .F. ) ;
#26649=VECTOR ( 'NONE', #8429, 1000.000000000000000 ) ;
#26663=ORIENTED_EDGE ( 'NONE', *, *, #33811, .T. ) ;
#26668=ORIENTED_EDGE ( 'NONE', *, *, #23077, .T. ) ;
#26685=ORIENTED_EDGE ( 'NONE', *, *, #5523, .F. ) ;
#26749=EDGE_LOOP ( 'NONE', ( #1793, #29734, #661, #29986 ) ) ;
#26786=FILL_AREA_STYLE ('',( #20781 ) ) ;
#26857=DIRECTION ( 'NONE',  ( 0.000000000000000000, -1.000000000000000000, 0.000000000000000000 ) ) ;
#26944=ORIENTED_EDGE ( 'NONE', *, *, #13769, .F. ) ;
#26945=EDGE_CURVE ( 'NONE', #28371, #26995, #24872, .T. ) ;
#26995=VERTEX_POINT ( 'NONE', #30844 ) ;
#27096=ORIENTED_EDGE ( 'NONE', *, *, #23077, .F. ) ;
#27133=ORIENTED_EDGE ( 'NONE', *, *, #33811, .F. ) ;
#27173=DIRECTION ( 'NONE',  ( -1.000000000000000000, -0.000000000000000000, -0.000000000000000000 ) ) ;
#27180=CARTESIAN_POINT ( 'NONE',  ( 0.000000000000000000, 0.000000000000000000, 0.000000000000000000 ) ) ;
#27301=AXIS2_PLACEMENT_3D ( 'NONE', #24148, #21705, #35603 ) ;
#27307=CIRCLE ( 'NONE', #17727, 2.541999999999999815 ) ;
#27310=AXIS2_PLACEMENT_3D ( 'NONE', #9965, #21409, #32852 ) ;
#27318=VECTOR ( 'NONE', #3703, 1000.000000000000000 ) ;
#27353=ORIENTED_EDGE ( 'NONE', *, *, #36770, .T. ) ;
#27440=CIRCLE ( 'NONE', #13688, 3.000000000000000444 ) ;
#27575=PRODUCT_DEFINITION_CONTEXT ( 'detailed design', #316, 'design' ) ;
#27577=DIRECTION ( 'NONE',  ( 0.000000000000000000, 0.000000000000000000, -1.000000000000000000 ) ) ;
#27578=ORIENTED_EDGE ( 'NONE', *, *, #7539, .T. ) ;
#27581=VECTOR ( 'NONE', #24366, 1000.000000000000000 ) ;
#27634=CIRCLE ( 'NONE', #4304, 2.541999999999999815 ) ;
#27635=PLANE ( 'NONE',  #25360 ) ;
#27656=EDGE_CURVE ( 'NONE', #26265, #16950, #23710, .T. ) ;
#27784=AXIS2_PLACEMENT_3D ( 'NONE', #10895, #10177, #24980 ) ;
#27817=ORIENTED_EDGE ( 'NONE', *, *, #34282, .T. ) ;
#27857=VECTOR ( 'NONE', #8167, 1000.000000000000000 ) ;
#27866=CARTESIAN_POINT ( 'NONE',  ( 3.000000000000000000, -1.467624384280032501, -2.541999999999998483 ) ) ;
#27919=AXIS2_PLACEMENT_3D ( 'NONE', #28931, #23690, #3258 ) ;
#27994=STYLED_ITEM ( 'NONE', ( #3353 ), #17512 ) ;
#28001=CARTESIAN_POINT ( 'NONE',  ( 3.000000000000000000, -1.467624384280027172, 2.542000000000001592 ) ) ;
#28186=DIRECTION ( 'NONE',  ( 1.000000000000000000, 0.000000000000000000, 0.000000000000000000 ) ) ;
#28227=ORIENTED_EDGE ( 'NONE', *, *, #11407, .T. ) ;
#28284=CIRCLE ( 'NONE', #33081, 3.250000000000001332 ) ;
#28293=EDGE_LOOP ( 'NONE', ( #5641, #36038, #3142, #34748 ) ) ;
#28349=FACE_OUTER_BOUND ( 'NONE', #30395, .T. ) ;
#28351=ORIENTED_EDGE ( 'NONE', *, *, #33669, .F. ) ;
#28371=VERTEX_POINT ( 'NONE', #7423 ) ;
#28391=LINE ( 'NONE', #2166, #13485 ) ;
#28557=CARTESIAN_POINT ( 'NONE',  ( 0.000000000000000000, -2.935248768560059229, 3.469446951953614189E-15 ) ) ;
#28662=CARTESIAN_POINT ( 'NONE',  ( -31.74999999999995737, 0.000000000000000000, 5.000000000000000000 ) ) ;
#28734=DIRECTION ( 'NONE',  ( 0.000000000000000000, 0.000000000000000000, 1.000000000000000000 ) ) ;
#28746=LINE ( 'NONE', #20308, #16366 ) ;
#28759=VERTEX_POINT ( 'NONE', #10380 ) ;
#28868=ADVANCED_FACE ( 'NONE', ( #37008 ), #22561, .T. ) ;
#28931=CARTESIAN_POINT ( 'NONE',  ( 66.00000000000000000, 0.000000000000000000, 0.000000000000000000 ) ) ;
#29120=EDGE_CURVE ( 'NONE', #26265, #34844, #2185, .T. ) ;
#29151=DIRECTION ( 'NONE',  ( -1.000000000000000000, -0.000000000000000000, -0.000000000000000000 ) ) ;
#29175=AXIS2_PLACEMENT_3D ( 'NONE', #16703, #7704, #16325 ) ;
#29178=EDGE_LOOP ( 'NONE', ( #27096, #26644, #22489, #10834, #4277 ) ) ;
#29181=SHAPE_DEFINITION_REPRESENTATION ( #5561, #33015 ) ;
#29223=( NAMED_UNIT ( * ) SI_UNIT ( $, .STERADIAN. ) SOLID_ANGLE_UNIT ( ) );
#29229=ORIENTED_EDGE ( 'NONE', *, *, #29120, .F. ) ;
#29258=DIRECTION ( 'NONE',  ( 0.000000000000000000, 0.5000000000000011102, 0.8660254037844379305 ) ) ;
#29339=EDGE_CURVE ( 'NONE', #28759, #24614, #8769, .T. ) ;
#29372=PRODUCT_CONTEXT ( 'NONE', #13462, 'mechanical' ) ;
#29386=CARTESIAN_POINT ( 'NONE',  ( 3.000000000000000000, 1.467624384280024730, -2.542000000000001592 ) ) ;
#29392=ORIENTED_EDGE ( 'NONE', *, *, #32637, .T. ) ;
#29597=LINE ( 'NONE', #18167, #35258 ) ;
#29666=EDGE_LOOP ( 'NONE', ( #27353, #13904, #1229, #11596, #31553 ) ) ;
#29734=ORIENTED_EDGE ( 'NONE', *, *, #9003, .T. ) ;
#29808=CARTESIAN_POINT ( 'NONE',  ( 5.999999999999998224, 0.000000000000000000, 0.000000000000000000 ) ) ;
#29812=VECTOR ( 'NONE', #14299, 1000.000000000000000 ) ;
#29938=CIRCLE ( 'NONE', #7819, 0.2500000000000002220 ) ;
#29986=ORIENTED_EDGE ( 'NONE', *, *, #32210, .F. ) ;
#30062=VERTEX_POINT ( 'NONE', #28557 ) ;
#30073=DIRECTION ( 'NONE',  ( -1.000000000000000000, -0.000000000000000000, -0.000000000000000000 ) ) ;
#30119=ORIENTED_EDGE ( 'NONE', *, *, #11581, .T. ) ;
#30190=ADVANCED_FACE ( 'NONE', ( #979 ), #35495, .F. ) ;
#30288=AXIS2_PLACEMENT_3D ( 'NONE', #1521, #26857, #1172 ) ;
#30308=ORIENTED_EDGE ( 'NONE', *, *, #19084, .F. ) ;
#30313=AXIS2_PLACEMENT_3D ( 'NONE', #920, #26431, #17998 ) ;
#30384=DIRECTION ( 'NONE',  ( 0.000000000000000000, 0.000000000000000000, 1.000000000000000000 ) ) ;
#30395=EDGE_LOOP ( 'NONE', ( #23892, #4441, #33429, #34025 ) ) ;
#30457=VECTOR ( 'NONE', #11409, 1000.000000000000114 ) ;
#30489=VECTOR ( 'NONE', #14035, 1000.000000000000000 ) ;
#30531=DIRECTION ( 'NONE',  ( 0.000000000000000000, -0.5000000000000011102, -0.8660254037844379305 ) ) ;
#30600=VERTEX_POINT ( 'NONE', #33975 ) ;
#30648=EDGE_CURVE ( 'NONE', #6013, #12103, #22521, .T. ) ;
#30660=DIRECTION ( 'NONE',  ( 1.000000000000000000, 0.000000000000000000, 0.000000000000000000 ) ) ;
#30844=CARTESIAN_POINT ( 'NONE',  ( 6.249999999999998224, 0.000000000000000000, 3.000000000000000888 ) ) ;
#30891=EDGE_CURVE ( 'NONE', #28371, #30600, #2334, .T. ) ;
#30969=EDGE_CURVE ( 'NONE', #34463, #30062, #2793, .T. ) ;
#31080=EDGE_LOOP ( 'NONE', ( #8003, #33753, #18642, #26685 ) ) ;
#31152=VECTOR ( 'NONE', #20476, 1000.000000000000000 ) ;
#31250=ORIENTED_EDGE ( 'NONE', *, *, #22119, .F. ) ;
#31307=( NAMED_UNIT ( * ) PLANE_ANGLE_UNIT ( ) SI_UNIT ( $, .RADIAN. ) );
#31346=ADVANCED_FACE ( 'NONE', ( #5556 ), #36521, .F. ) ;
#31357=ADVANCED_FACE ( 'NONE', ( #25634 ), #21780, .F. ) ;
#31411=DIRECTION ( 'NONE',  ( 1.000000000000000000, 0.000000000000000000, 0.000000000000000000 ) ) ;
#31440=ORIENTED_EDGE ( 'NONE', *, *, #27656, .T. ) ;
#31509=VECTOR ( 'NONE', #2143, 1000.000000000000000 ) ;
#31553=ORIENTED_EDGE ( 'NONE', *, *, #19629, .T. ) ;
#31681=( NAMED_UNIT ( * ) SI_UNIT ( $, .STERADIAN. ) SOLID_ANGLE_UNIT ( ) );
#31797=PLANE ( 'NONE',  #20972 ) ;
#31858=PLANE ( 'NONE',  #35011 ) ;
#31863=EDGE_LOOP ( 'NONE', ( #6564, #23670 ) ) ;
#31867=ADVANCED_FACE ( 'NONE', ( #34720 ), #31858, .F. ) ;
#31888=DIRECTION ( 'NONE',  ( -0.5000000000000051070, 0.000000000000000000, 0.8660254037844355990 ) ) ;
#31893=CARTESIAN_POINT ( 'NONE',  ( 5.999999999999998224, 0.000000000000000000, 5.000000000000000000 ) ) ;
#31922=AXIS2_PLACEMENT_3D ( 'NONE', #4749, #12975, #15991 ) ;
#32027=ORIENTED_EDGE ( 'NONE', *, *, #34134, .F. ) ;
#32049=AXIS2_PLACEMENT_3D ( 'NONE', #36638, #5504, #8499 ) ;
#32083=EDGE_CURVE ( 'NONE', #30600, #1512, #11676, .T. ) ;
#32149=ORIENTED_EDGE ( 'NONE', *, *, #19898, .F. ) ;
#32210=EDGE_CURVE ( 'NONE', #19159, #26265, #36569, .T. ) ;
#32265=ORIENTED_EDGE ( 'NONE', *, *, #18601, .T. ) ;
#32309=ORIENTED_EDGE ( 'NONE', *, *, #19084, .T. ) ;
#32349=ADVANCED_FACE ( 'NONE', ( #12513 ), #35026, .F. ) ;
#32428=CYLINDRICAL_SURFACE ( 'NONE', #4266, 3.000000000000000888 ) ;
#32453=EDGE_LOOP ( 'NONE', ( #27133, #9709, #19353, #27578, #8060 ) ) ;
#32467=FACE_OUTER_BOUND ( 'NONE', #18849, .T. ) ;
#32476=DIRECTION ( 'NONE',  ( -1.000000000000000000, -0.000000000000000000, -0.000000000000000000 ) ) ;
#32486=CARTESIAN_POINT ( 'NONE',  ( 0.000000000000000000, 1.467624384280024730, -2.542000000000001592 ) ) ;
#32608=LINE ( 'NONE', #26258, #265 ) ;
#32637=EDGE_CURVE ( 'NONE', #16950, #9855, #5734, .T. ) ;
#32668=AXIS2_PLACEMENT_3D ( 'NONE', #25978, #35379, #34621 ) ;
#32824=EDGE_CURVE ( 'NONE', #22858, #20479, #18268, .T. ) ;
#32852=DIRECTION ( 'NONE',  ( 0.000000000000000000, 0.000000000000000000, 1.000000000000000000 ) ) ;
#32888=CARTESIAN_POINT ( 'NONE',  ( 65.44550000000002399, 3.673940397442060361E-16, -3.000000000000000444 ) ) ;
#32952=AXIS2_PLACEMENT_3D ( 'NONE', #21941, #36025, #27577 ) ;
#33015=SHAPE_REPRESENTATION ( 'socket head cap screw_iso_ISO 4762 M6 x 60 - 24N', ( #21385 ), #2251 ) ;
#33029=LINE ( 'NONE', #1904, #12105 ) ;
#33035=EDGE_LOOP ( 'NONE', ( #12533, #21507, #31250 ) ) ;
#33081=AXIS2_PLACEMENT_3D ( 'NONE', #12412, #32476, #14505 ) ;
#33109=VERTEX_POINT ( 'NONE', #34761 ) ;
#33115=VECTOR ( 'NONE', #29151, 1000.000000000000000 ) ;
#33237=AXIS2_PLACEMENT_3D ( 'NONE', #24750, #27173, #22131 ) ;
#33297=LINE ( 'NONE', #2716, #27857 ) ;
#33372=VECTOR ( 'NONE', #4777, 1000.000000000000114 ) ;
#33387=ADVANCED_FACE ( 'NONE', ( #2642 ), #9357, .T. ) ;
#33411=ADVANCED_FACE ( 'NONE', ( #25524 ), #13895, .T. ) ;
#33429=ORIENTED_EDGE ( 'NONE', *, *, #32637, .F. ) ;
#33669=EDGE_CURVE ( 'NONE', #19159, #22352, #16014, .T. ) ;
#33753=ORIENTED_EDGE ( 'NONE', *, *, #9481, .T. ) ;
#33768=TOROIDAL_SURFACE ( 'NONE', #27784, 3.250000000000001332, 0.2500000000000000000 ) ;
#33774=EDGE_LOOP ( 'NONE', ( #16259, #5200, #36900 ) ) ;
#33811=EDGE_CURVE ( 'NONE', #35409, #12497, #19483, .T. ) ;
#33817=AXIS2_PLACEMENT_3D ( 'NONE', #26040, #23045, #18154 ) ;
#33821=DIRECTION ( 'NONE',  ( 1.000000000000000000, 0.000000000000000000, 0.000000000000000000 ) ) ;
#33975=CARTESIAN_POINT ( 'NONE',  ( 5.999999999999999112, 0.000000000000000000, -3.250000000000001332 ) ) ;
#34025=ORIENTED_EDGE ( 'NONE', *, *, #27656, .F. ) ;
#34067=DIRECTION ( 'NONE',  ( 0.000000000000000000, 0.000000000000000000, -1.000000000000000000 ) ) ;
#34119=CARTESIAN_POINT ( 'NONE',  ( -31.74999999999995737, 0.000000000000000000, 3.000000000000000888 ) ) ;
#34134=EDGE_CURVE ( 'NONE', #22352, #19159, #25629, .T. ) ;
#34156=PRESENTATION_STYLE_ASSIGNMENT (( #11602 ) ) ;
#34165=CARTESIAN_POINT ( 'NONE',  ( 0.000000000000000000, 0.000000000000000000, 0.000000000000000000 ) ) ;
#34240=DIRECTION ( 'NONE',  ( 0.000000000000000000, 0.000000000000000000, 1.000000000000000000 ) ) ;
#34282=EDGE_CURVE ( 'NONE', #8433, #6013, #13944, .T. ) ;
#34331=DIRECTION ( 'NONE',  ( 0.000000000000000000, -0.4999999999999996114, 0.8660254037844388186 ) ) ;
#34411=DIRECTION ( 'NONE',  ( -1.000000000000000000, -0.000000000000000000, -0.000000000000000000 ) ) ;
#34463=VERTEX_POINT ( 'NONE', #3792 ) ;
#34466=EDGE_CURVE ( 'NONE', #1512, #30600, #28284, .T. ) ;
#34527=ORIENTED_EDGE ( 'NONE', *, *, #5523, .T. ) ;
#34621=DIRECTION ( 'NONE',  ( 0.000000000000000000, 0.000000000000000000, 1.000000000000000000 ) ) ;
#34720=FACE_OUTER_BOUND ( 'NONE', #33035, .T. ) ;
#34748=ORIENTED_EDGE ( 'NONE', *, *, #29120, .T. ) ;
#34761=CARTESIAN_POINT ( 'NONE',  ( 3.000000000000000000, 2.201436576420041202, -1.271000000000003460 ) ) ;
#34844=VERTEX_POINT ( 'NONE', #20615 ) ;
#34859=( NAMED_UNIT ( * ) PLANE_ANGLE_UNIT ( ) SI_UNIT ( $, .RADIAN. ) );
#34899=DIRECTION ( 'NONE',  ( -1.000000000000000000, 0.000000000000000000, -0.000000000000000000 ) ) ;
#34901=DIRECTION ( 'NONE',  ( -1.000000000000000000, -0.000000000000000000, -0.000000000000000000 ) ) ;
#35011=AXIS2_PLACEMENT_3D ( 'NONE', #4142, #3389, #26267 ) ;
#35026=PLANE ( 'NONE',  #18272 ) ;
#35038=( LENGTH_UNIT ( ) NAMED_UNIT ( * ) SI_UNIT ( .MILLI., .METRE. ) );
#35258=VECTOR ( 'NONE', #15174, 1000.000000000000000 ) ;
#35379=DIRECTION ( 'NONE',  ( -1.000000000000000000, -0.000000000000000000, -0.000000000000000000 ) ) ;
#35391=AXIS2_PLACEMENT_3D ( 'NONE', #4912, #14815, #20065 ) ;
#35409=VERTEX_POINT ( 'NONE', #18710 ) ;
#35432=( NAMED_UNIT ( * ) SI_UNIT ( $, .STERADIAN. ) SOLID_ANGLE_UNIT ( ) );
#35464=PLANE ( 'NONE',  #19852 ) ;
#35495=PLANE ( 'NONE',  #15441 ) ;
#35516=CIRCLE ( 'NONE', #24728, 5.000000000000000000 ) ;
#35518=CARTESIAN_POINT ( 'NONE',  ( 3.000000000000000000, 1.467624384280024730, -2.542000000000001592 ) ) ;
#35536=EDGE_LOOP ( 'NONE', ( #23258, #26663, #25182, #23594, #120 ) ) ;
#35603=DIRECTION ( 'NONE',  ( 0.000000000000000000, 0.4999999999999997224, -0.8660254037844388186 ) ) ;
#35709=( GEOMETRIC_REPRESENTATION_CONTEXT ( 3 ) GLOBAL_UNCERTAINTY_ASSIGNED_CONTEXT ( ( #1318 ) ) GLOBAL_UNIT_ASSIGNED_CONTEXT ( ( #23595, #34859, #29223 ) ) REPRESENTATION_CONTEXT ( 'NONE', 'WORKASPACE' ) );
#35746=LINE ( 'NONE', #36109, #2194 ) ;
#35756=ORIENTED_EDGE ( 'NONE', *, *, #9481, .F. ) ;
#35758=CARTESIAN_POINT ( 'NONE',  ( 3.000000000000000000, -2.935248768560059229, 3.469446951953614189E-15 ) ) ;
#35786=DIRECTION ( 'NONE',  ( -1.000000000000000000, -0.000000000000000000, -0.000000000000000000 ) ) ;
#35795=ORIENTED_EDGE ( 'NONE', *, *, #23547, .T. ) ;
#35947=PLANE ( 'NONE',  #5123 ) ;
#35986=FACE_OUTER_BOUND ( 'NONE', #10530, .T. ) ;
#36025=DIRECTION ( 'NONE',  ( 1.000000000000000000, 0.000000000000000000, 0.000000000000000000 ) ) ;
#36038=ORIENTED_EDGE ( 'NONE', *, *, #34134, .T. ) ;
#36109=CARTESIAN_POINT ( 'NONE',  ( 0.000000000000000000, -1.467624384280027172, 2.542000000000001592 ) ) ;
#36118=DIRECTION ( 'NONE',  ( 0.000000000000000000, 1.224646799147351482E-16, 1.000000000000000000 ) ) ;
#36176=CARTESIAN_POINT ( 'NONE',  ( 0.000000000000000000, -1.467624384280032501, -2.541999999999998483 ) ) ;
#36243=ORIENTED_EDGE ( 'NONE', *, *, #6993, .F. ) ;
#36283=DIRECTION ( 'NONE',  ( 0.000000000000000000, 0.000000000000000000, 1.000000000000000000 ) ) ;
#36302=VECTOR ( 'NONE', #13020, 1000.000000000000114 ) ;
#36327=PRODUCT_DEFINITION_FORMATION_WITH_SPECIFIED_SOURCE ( 'ANY', '', #11249, .NOT_KNOWN. ) ;
#36345=CIRCLE ( 'NONE', #27919, 2.445500000000000007 ) ;
#36381=ADVANCED_FACE ( 'NONE', ( #14763 ), #18327, .F. ) ;
#36396=DIRECTION ( 'NONE',  ( 1.000000000000000000, 0.000000000000000000, 0.000000000000000000 ) ) ;
#36442=EDGE_CURVE ( 'NONE', #14753, #12497, #3874, .T. ) ;
#36477=EDGE_LOOP ( 'NONE', ( #22998, #26944, #1783 ) ) ;
#36521=PLANE ( 'NONE',  #24794 ) ;
#36569=LINE ( 'NONE', #28662, #26649 ) ;
#36575=UNCERTAINTY_MEASURE_WITH_UNIT (LENGTH_MEASURE( 1.000000000000000082E-05 ), #26051, 'distance_accuracy_value', 'NONE');
#36579=TOROIDAL_SURFACE ( 'NONE', #35391, 3.250000000000001332, 0.2500000000000000000 ) ;
#36623=LINE ( 'NONE', #16753, #29812 ) ;
#36630=DIRECTION ( 'NONE',  ( 0.000000000000000000, 0.000000000000000000, 1.000000000000000000 ) ) ;
#36638=CARTESIAN_POINT ( 'NONE',  ( 3.000000000000000000, -2.935248768560059229, 3.469446951953614189E-15 ) ) ;
#36647=CARTESIAN_POINT ( 'NONE',  ( 0.3000000000000016542, 0.000000000000000000, 0.000000000000000000 ) ) ;
#36663=CARTESIAN_POINT ( 'NONE',  ( 66.00000000000000000, 0.000000000000000000, 0.000000000000000000 ) ) ;
#36770=EDGE_CURVE ( 'NONE', #34463, #12103, #35746, .T. ) ;
#36864=CIRCLE ( 'NONE', #20680, 0.2999999999999999334 ) ;
#36900=ORIENTED_EDGE ( 'NONE', *, *, #3188, .F. ) ;
#36985=CIRCLE ( 'NONE', #19036, 3.000000000000000888 ) ;
#37008=FACE_OUTER_BOUND ( 'NONE', #29178, .T. ) ;
#37050=CARTESIAN_POINT ( 'NONE',  ( 3.000000000000000000, 0.000000000000000000, 0.000000000000000000 ) ) ;
ENDSEC;
END-ISO-10303-21;
